ISO-10303-21;
HEADER;
/* Generated by software containing ST-Developer
 * from STEP Tools, Inc. (www.steptools.com) 
 */

FILE_DESCRIPTION(
/* description */ ('Rotary union on bearing shaft'),
/* implementation_level */ '2;1');

FILE_NAME(
/* name */ 'Bonded foot pad (1).step',
/* time_stamp */ '2026-10-28T03:24:01-07:00',
/* author */ (''),
/* organization */ (''),
/* preprocessor_version */ 'ST-DEVELOPER v20.2',
/* originating_system */ 'Autodesk Translation Framework v15.17.0.0',
/* authorisation */ '');

FILE_SCHEMA (('AUTOMOTIVE_DESIGN { 1 0 10303 214 3 1 1 }'));
ENDSEC;

DATA;
#10=MECHANICAL_DESIGN_GEOMETRIC_PRESENTATION_REPRESENTATION('',(#323),#9448);
#269=SHAPE_REPRESENTATION_RELATIONSHIP('SRR','None',#9569,#296);
#296=ADVANCED_BREP_SHAPE_REPRESENTATION('',(#358),#9429);
#323=STYLED_ITEM('',(#9771),#358);
#358=MANIFOLD_SOLID_BREP('Body1',#4878);
#544=PLANE('',#5421);
#545=PLANE('',#5422);
#546=PLANE('',#5423);
#547=PLANE('',#5424);
#548=PLANE('',#5425);
#549=PLANE('',#5426);
#761=FACE_OUTER_BOUND('',#1124,.T.);
#762=FACE_OUTER_BOUND('',#1125,.T.);
#763=FACE_OUTER_BOUND('',#1126,.T.);
#764=FACE_OUTER_BOUND('',#1127,.T.);
#765=FACE_OUTER_BOUND('',#1128,.T.);
#766=FACE_OUTER_BOUND('',#1129,.T.);
#1124=EDGE_LOOP('',(#3699,#3700,#3701,#3702));
#1125=EDGE_LOOP('',(#3703,#3704,#3705,#3706));
#1126=EDGE_LOOP('',(#3707,#3708,#3709,#3710));
#1127=EDGE_LOOP('',(#3711,#3712,#3713,#3714));
#1128=EDGE_LOOP('',(#3715,#3716,#3717,#3718));
#1129=EDGE_LOOP('',(#3719,#3720,#3721,#3722));
#1470=LINE('',#8005,#1790);
#1471=LINE('',#8007,#1791);
#1472=LINE('',#8009,#1792);
#1473=LINE('',#8010,#1793);
#1474=LINE('',#8013,#1794);
#1475=LINE('',#8015,#1795);
#1476=LINE('',#8016,#1796);
#1477=LINE('',#8019,#1797);
#1478=LINE('',#8021,#1798);
#1479=LINE('',#8022,#1799);
#1480=LINE('',#8024,#1800);
#1481=LINE('',#8025,#1801);
#1790=VECTOR('',#6373,1.);
#1791=VECTOR('',#6374,1.);
#1792=VECTOR('',#6375,1.);
#1793=VECTOR('',#6376,1.);
#1794=VECTOR('',#6379,1.);
#1795=VECTOR('',#6380,1.);
#1796=VECTOR('',#6381,1.);
#1797=VECTOR('',#6384,1.);
#1798=VECTOR('',#6385,1.);
#1799=VECTOR('',#6386,1.);
#1800=VECTOR('',#6389,1.);
#1801=VECTOR('',#6390,1.);
#2396=VERTEX_POINT('',#8003);
#2397=VERTEX_POINT('',#8004);
#2398=VERTEX_POINT('',#8006);
#2399=VERTEX_POINT('',#8008);
#2400=VERTEX_POINT('',#8012);
#2401=VERTEX_POINT('',#8014);
#2402=VERTEX_POINT('',#8018);
#2403=VERTEX_POINT('',#8020);
#2877=EDGE_CURVE('',#2396,#2397,#1470,.T.);
#2878=EDGE_CURVE('',#2397,#2398,#1471,.T.);
#2879=EDGE_CURVE('',#2399,#2398,#1472,.T.);
#2880=EDGE_CURVE('',#2396,#2399,#1473,.T.);
#2881=EDGE_CURVE('',#2400,#2396,#1474,.T.);
#2882=EDGE_CURVE('',#2401,#2399,#1475,.T.);
#2883=EDGE_CURVE('',#2400,#2401,#1476,.T.);
#2884=EDGE_CURVE('',#2402,#2400,#1477,.T.);
#2885=EDGE_CURVE('',#2403,#2401,#1478,.T.);
#2886=EDGE_CURVE('',#2402,#2403,#1479,.T.);
#2887=EDGE_CURVE('',#2397,#2402,#1480,.T.);
#2888=EDGE_CURVE('',#2398,#2403,#1481,.T.);
#3699=ORIENTED_EDGE('',*,*,#2877,.T.);
#3700=ORIENTED_EDGE('',*,*,#2878,.T.);
#3701=ORIENTED_EDGE('',*,*,#2879,.F.);
#3702=ORIENTED_EDGE('',*,*,#2880,.F.);
#3703=ORIENTED_EDGE('',*,*,#2881,.T.);
#3704=ORIENTED_EDGE('',*,*,#2880,.T.);
#3705=ORIENTED_EDGE('',*,*,#2882,.F.);
#3706=ORIENTED_EDGE('',*,*,#2883,.F.);
#3707=ORIENTED_EDGE('',*,*,#2884,.T.);
#3708=ORIENTED_EDGE('',*,*,#2883,.T.);
#3709=ORIENTED_EDGE('',*,*,#2885,.F.);
#3710=ORIENTED_EDGE('',*,*,#2886,.F.);
#3711=ORIENTED_EDGE('',*,*,#2887,.T.);
#3712=ORIENTED_EDGE('',*,*,#2886,.T.);
#3713=ORIENTED_EDGE('',*,*,#2888,.F.);
#3714=ORIENTED_EDGE('',*,*,#2878,.F.);
#3715=ORIENTED_EDGE('',*,*,#2888,.T.);
#3716=ORIENTED_EDGE('',*,*,#2885,.T.);
#3717=ORIENTED_EDGE('',*,*,#2882,.T.);
#3718=ORIENTED_EDGE('',*,*,#2879,.T.);
#3719=ORIENTED_EDGE('',*,*,#2887,.F.);
#3720=ORIENTED_EDGE('',*,*,#2877,.F.);
#3721=ORIENTED_EDGE('',*,*,#2881,.F.);
#3722=ORIENTED_EDGE('',*,*,#2884,.F.);
#4674=ADVANCED_FACE('',(#761),#544,.T.);
#4675=ADVANCED_FACE('',(#762),#545,.T.);
#4676=ADVANCED_FACE('',(#763),#546,.T.);
#4677=ADVANCED_FACE('',(#764),#547,.T.);
#4678=ADVANCED_FACE('',(#765),#548,.T.);
#4679=ADVANCED_FACE('',(#766),#549,.F.);
#4878=CLOSED_SHELL('',(#4674,#4675,#4676,#4677,#4678,#4679));
#5420=AXIS2_PLACEMENT_3D('',#8001,#6369,#6370);
#5421=AXIS2_PLACEMENT_3D('',#8002,#6371,#6372);
#5422=AXIS2_PLACEMENT_3D('',#8011,#6377,#6378);
#5423=AXIS2_PLACEMENT_3D('',#8017,#6382,#6383);
#5424=AXIS2_PLACEMENT_3D('',#8023,#6387,#6388);
#5425=AXIS2_PLACEMENT_3D('',#8026,#6391,#6392);
#5426=AXIS2_PLACEMENT_3D('',#8027,#6393,#6394);
#6369=DIRECTION('axis',(0.,0.,1.));
#6370=DIRECTION('refdir',(1.,0.,0.));
#6371=DIRECTION('center_axis',(0.,1.,0.));
#6372=DIRECTION('ref_axis',(-1.,0.,0.));
#6373=DIRECTION('',(-1.,0.,0.));
#6374=DIRECTION('',(0.,0.,1.));
#6375=DIRECTION('',(-1.,0.,0.));
#6376=DIRECTION('',(0.,0.,1.));
#6377=DIRECTION('center_axis',(1.,0.,0.));
#6378=DIRECTION('ref_axis',(0.,1.,0.));
#6379=DIRECTION('',(0.,1.,0.));
#6380=DIRECTION('',(0.,1.,0.));
#6381=DIRECTION('',(0.,0.,1.));
#6382=DIRECTION('center_axis',(0.,-1.,0.));
#6383=DIRECTION('ref_axis',(1.,0.,0.));
#6384=DIRECTION('',(1.,0.,0.));
#6385=DIRECTION('',(1.,0.,0.));
#6386=DIRECTION('',(0.,0.,1.));
#6387=DIRECTION('center_axis',(-1.,0.,0.));
#6388=DIRECTION('ref_axis',(0.,-1.,0.));
#6389=DIRECTION('',(0.,-1.,0.));
#6390=DIRECTION('',(0.,-1.,0.));
#6391=DIRECTION('center_axis',(0.,0.,1.));
#6392=DIRECTION('ref_axis',(1.,0.,0.));
#6393=DIRECTION('center_axis',(0.,0.,1.));
#6394=DIRECTION('ref_axis',(1.,0.,0.));
#8001=CARTESIAN_POINT('',(0.,0.,0.));
#8002=CARTESIAN_POINT('Origin',(5.5,7.,-0.3));
#8003=CARTESIAN_POINT('',(5.5,7.,-0.3));
#8004=CARTESIAN_POINT('',(-5.5,7.,-0.3));
#8005=CARTESIAN_POINT('',(5.5,7.,-0.3));
#8006=CARTESIAN_POINT('',(-5.5,7.,0.));
#8007=CARTESIAN_POINT('',(-5.5,7.,-0.3));
#8008=CARTESIAN_POINT('',(5.5,7.,0.));
#8009=CARTESIAN_POINT('',(5.5,7.,0.));
#8010=CARTESIAN_POINT('',(5.5,7.,-0.3));
#8011=CARTESIAN_POINT('Origin',(5.5,6.,-0.3));
#8012=CARTESIAN_POINT('',(5.5,6.,-0.3));
#8013=CARTESIAN_POINT('',(5.5,6.,-0.3));
#8014=CARTESIAN_POINT('',(5.5,6.,0.));
#8015=CARTESIAN_POINT('',(5.5,6.,0.));
#8016=CARTESIAN_POINT('',(5.5,6.,-0.3));
#8017=CARTESIAN_POINT('Origin',(-5.5,6.,-0.3));
#8018=CARTESIAN_POINT('',(-5.5,6.,-0.3));
#8019=CARTESIAN_POINT('',(-5.5,6.,-0.3));
#8020=CARTESIAN_POINT('',(-5.5,6.,0.));
#8021=CARTESIAN_POINT('',(-5.5,6.,0.));
#8022=CARTESIAN_POINT('',(-5.5,6.,-0.3));
#8023=CARTESIAN_POINT('Origin',(-5.5,7.,-0.3));
#8024=CARTESIAN_POINT('',(-5.5,7.,-0.3));
#8025=CARTESIAN_POINT('',(-5.5,7.,0.));
#8026=CARTESIAN_POINT('Origin',(0.,6.5,0.));
#8027=CARTESIAN_POINT('Origin',(0.,6.5,-0.3));
#9397=UNCERTAINTY_MEASURE_WITH_UNIT(LENGTH_MEASURE(0.001),#9449,
'DISTANCE_ACCURACY_VALUE',
'Maximum model space distance between geometric entities at asserted c
onnectivities');
#9416=UNCERTAINTY_MEASURE_WITH_UNIT(LENGTH_MEASURE(0.001),#9449,
'DISTANCE_ACCURACY_VALUE',
'Maximum model space distance between geometric entities at asserted c
onnectivities');
#9429=(
GEOMETRIC_REPRESENTATION_CONTEXT(3)
GLOBAL_UNCERTAINTY_ASSIGNED_CONTEXT((#9397))
GLOBAL_UNIT_ASSIGNED_CONTEXT((#9449,#9451,#9452))
REPRESENTATION_CONTEXT('','3D')
);
#9448=(
GEOMETRIC_REPRESENTATION_CONTEXT(3)
GLOBAL_UNCERTAINTY_ASSIGNED_CONTEXT((#9416))
GLOBAL_UNIT_ASSIGNED_CONTEXT((#9449,#9451,#9452))
REPRESENTATION_CONTEXT('','3D')
);
#9449=(
LENGTH_UNIT()
NAMED_UNIT(*)
SI_UNIT(.CENTI.,.METRE.)
);
#9451=(
NAMED_UNIT(*)
PLANE_ANGLE_UNIT()
SI_UNIT($,.RADIAN.)
);
#9452=(
NAMED_UNIT(*)
SI_UNIT($,.STERADIAN.)
SOLID_ANGLE_UNIT()
);
#9465=SHAPE_DEFINITION_REPRESENTATION(#9496,#9569);
#9496=PRODUCT_DEFINITION_SHAPE('',$,#9601);
#9569=SHAPE_REPRESENTATION('',(#5420),#9429);
#9588=PRODUCT_DEFINITION_CONTEXT('part definition',#9683,'design');
#9601=PRODUCT_DEFINITION('Bonded foot pad (1)','Bonded foot pad (1)',#9632,
#9588);
#9632=PRODUCT_DEFINITION_FORMATION('',$,#9697);
#9683=APPLICATION_CONTEXT(
'Core Data for Automotive Mechanical Design Process');
#9684=PRODUCT_CONTEXT('part definition',#9683,'mechanical');
#9697=PRODUCT('Bonded foot pad (1)','Bonded foot pad (1)',
'Bonded foot pad (1)',(#9684));
#9765=COLOUR_RGB('Sky Blue',0.24,0.69,0.87);
#9766=FILL_AREA_STYLE_COLOUR('',#9765);
#9767=FILL_AREA_STYLE('',(#9766));
#9768=SURFACE_STYLE_FILL_AREA(#9767);
#9769=SURFACE_SIDE_STYLE('',(#9768));
#9770=SURFACE_STYLE_USAGE(.BOTH.,#9769);
#9771=PRESENTATION_STYLE_ASSIGNMENT((#9770));
ENDSEC;
END-ISO-10303-21;
